ISO-10303-21;
HEADER;
/* Generated by software containing ST-Developer
 * from STEP Tools, Inc. (www.steptools.com) 
 */

FILE_DESCRIPTION(
/* description */ (''),
/* implementation_level */ '2;1');

FILE_NAME(
/* name */ '07_Die_Magnet_D6x5_NdFeB.step',
/* time_stamp */ '2026-10-26T03:55:20-07:00',
/* author */ (''),
/* organization */ (''),
/* preprocessor_version */ 'ST-DEVELOPER v20.2',
/* originating_system */ 'Autodesk Translation Framework v15.15.0.0',
/* authorisation */ '');

FILE_SCHEMA (('AUTOMOTIVE_DESIGN { 1 0 10303 214 3 1 1 }'));
ENDSEC;

DATA;
#10=MECHANICAL_DESIGN_GEOMETRIC_PRESENTATION_REPRESENTATION('',(#181),#45236);
#141=SHAPE_REPRESENTATION_RELATIONSHIP('SRR','None',#45320,#161);
#161=ADVANCED_BREP_SHAPE_REPRESENTATION('',(#201),#45222);
#181=STYLED_ITEM('',(#45470),#201);
#201=MANIFOLD_SOLID_BREP('Body1',#16523);
#1134=PLANE('',#17166);
#1135=PLANE('',#17174);
#1683=CYLINDRICAL_SURFACE('',#17170,3.);
#2096=FACE_OUTER_BOUND('',#3096,.T.);
#2097=FACE_OUTER_BOUND('',#3097,.T.);
#2098=FACE_OUTER_BOUND('',#3098,.T.);
#2099=FACE_OUTER_BOUND('',#3099,.T.);
#2100=FACE_OUTER_BOUND('',#3100,.T.);
#3096=EDGE_LOOP('',(#12150));
#3097=EDGE_LOOP('',(#12151,#12152,#12153,#12154));
#3098=EDGE_LOOP('',(#12155,#12156,#12157,#12158));
#3099=EDGE_LOOP('',(#12159,#12160,#12161,#12162));
#3100=EDGE_LOOP('',(#12163));
#4168=LINE('',#32254,#5479);
#4169=LINE('',#32258,#5480);
#4170=LINE('',#32262,#5481);
#5479=VECTOR('',#19229,2.9);
#5480=VECTOR('',#19234,3.);
#5481=VECTOR('',#19239,2.9);
#6669=CIRCLE('',#17167,2.8);
#6670=CIRCLE('',#17169,3.);
#6671=CIRCLE('',#17171,3.);
#6672=CIRCLE('',#17173,2.8);
#7384=VERTEX_POINT('',#32249);
#7385=VERTEX_POINT('',#32252);
#7386=VERTEX_POINT('',#32256);
#7387=VERTEX_POINT('',#32260);
#9138=EDGE_CURVE('',#7384,#7384,#6669,.T.);
#9139=EDGE_CURVE('',#7385,#7385,#6670,.T.);
#9140=EDGE_CURVE('',#7385,#7384,#4168,.T.);
#9141=EDGE_CURVE('',#7386,#7386,#6671,.T.);
#9142=EDGE_CURVE('',#7386,#7385,#4169,.T.);
#9143=EDGE_CURVE('',#7387,#7387,#6672,.T.);
#9144=EDGE_CURVE('',#7387,#7386,#4170,.T.);
#12150=ORIENTED_EDGE('',*,*,#9138,.F.);
#12151=ORIENTED_EDGE('',*,*,#9139,.F.);
#12152=ORIENTED_EDGE('',*,*,#9140,.T.);
#12153=ORIENTED_EDGE('',*,*,#9138,.T.);
#12154=ORIENTED_EDGE('',*,*,#9140,.F.);
#12155=ORIENTED_EDGE('',*,*,#9141,.F.);
#12156=ORIENTED_EDGE('',*,*,#9142,.T.);
#12157=ORIENTED_EDGE('',*,*,#9139,.T.);
#12158=ORIENTED_EDGE('',*,*,#9142,.F.);
#12159=ORIENTED_EDGE('',*,*,#9143,.F.);
#12160=ORIENTED_EDGE('',*,*,#9144,.T.);
#12161=ORIENTED_EDGE('',*,*,#9141,.T.);
#12162=ORIENTED_EDGE('',*,*,#9144,.F.);
#12163=ORIENTED_EDGE('',*,*,#9143,.T.);
#15498=CONICAL_SURFACE('',#17168,2.9,0.785398163397449);
#15499=CONICAL_SURFACE('',#17172,2.9,0.785398163397448);
#15824=ADVANCED_FACE('',(#2096),#1134,.T.);
#15825=ADVANCED_FACE('',(#2097),#15498,.T.);
#15826=ADVANCED_FACE('',(#2098),#1683,.T.);
#15827=ADVANCED_FACE('',(#2099),#15499,.T.);
#15828=ADVANCED_FACE('',(#2100),#1135,.T.);
#16523=CLOSED_SHELL('',(#15824,#15825,#15826,#15827,#15828));
#17165=AXIS2_PLACEMENT_3D('',#32247,#19219,#19220);
#17166=AXIS2_PLACEMENT_3D('',#32248,#19221,#19222);
#17167=AXIS2_PLACEMENT_3D('',#32250,#19223,#19224);
#17168=AXIS2_PLACEMENT_3D('',#32251,#19225,#19226);
#17169=AXIS2_PLACEMENT_3D('',#32253,#19227,#19228);
#17170=AXIS2_PLACEMENT_3D('',#32255,#19230,#19231);
#17171=AXIS2_PLACEMENT_3D('',#32257,#19232,#19233);
#17172=AXIS2_PLACEMENT_3D('',#32259,#19235,#19236);
#17173=AXIS2_PLACEMENT_3D('',#32261,#19237,#19238);
#17174=AXIS2_PLACEMENT_3D('',#32263,#19240,#19241);
#19219=DIRECTION('axis',(0.,0.,1.));
#19220=DIRECTION('refdir',(1.,0.,0.));
#19221=DIRECTION('center_axis',(-1.,0.,0.));
#19222=DIRECTION('ref_axis',(0.,0.,1.));
#19223=DIRECTION('center_axis',(1.,0.,0.));
#19224=DIRECTION('ref_axis',(0.,0.,-1.));
#19225=DIRECTION('center_axis',(1.,0.,0.));
#19226=DIRECTION('ref_axis',(0.,1.,0.));
#19227=DIRECTION('center_axis',(1.,0.,0.));
#19228=DIRECTION('ref_axis',(0.,0.,-1.));
#19229=DIRECTION('',(-0.707106781186547,0.707106781186548,8.65956056235494E-17));
#19230=DIRECTION('center_axis',(1.,0.,0.));
#19231=DIRECTION('ref_axis',(0.,1.,0.));
#19232=DIRECTION('center_axis',(1.,0.,0.));
#19233=DIRECTION('ref_axis',(0.,0.,-1.));
#19234=DIRECTION('',(-1.,0.,0.));
#19235=DIRECTION('center_axis',(-1.,0.,0.));
#19236=DIRECTION('ref_axis',(0.,1.,0.));
#19237=DIRECTION('center_axis',(1.,0.,0.));
#19238=DIRECTION('ref_axis',(0.,0.,-1.));
#19239=DIRECTION('',(-0.707106781186548,-0.707106781186548,-8.65956056235493E-17));
#19240=DIRECTION('center_axis',(1.,0.,0.));
#19241=DIRECTION('ref_axis',(0.,0.,-1.));
#32247=CARTESIAN_POINT('',(0.,0.,0.));
#32248=CARTESIAN_POINT('Origin',(0.,2.8,0.));
#32249=CARTESIAN_POINT('',(1.73472347597681E-17,-2.8,-3.42901103761259E-16));
#32250=CARTESIAN_POINT('Origin',(0.,0.,0.));
#32251=CARTESIAN_POINT('Origin',(0.1,0.,0.));
#32252=CARTESIAN_POINT('',(0.2,-3.,-3.67394039744206E-16));
#32253=CARTESIAN_POINT('Origin',(0.2,0.,0.));
#32254=CARTESIAN_POINT('',(0.1,-2.9,-3.55147571752732E-16));
#32255=CARTESIAN_POINT('Origin',(2.5,0.,0.));
#32256=CARTESIAN_POINT('',(4.8,-3.,-3.67394039744206E-16));
#32257=CARTESIAN_POINT('Origin',(4.8,0.,0.));
#32258=CARTESIAN_POINT('',(2.5,-3.,-3.67394039744206E-16));
#32259=CARTESIAN_POINT('Origin',(4.9,0.,0.));
#32260=CARTESIAN_POINT('',(5.,-2.8,-3.42901103761259E-16));
#32261=CARTESIAN_POINT('Origin',(5.,0.,0.));
#32262=CARTESIAN_POINT('',(4.9,-2.9,-3.55147571752732E-16));
#32263=CARTESIAN_POINT('Origin',(5.,0.,0.));
#45200=UNCERTAINTY_MEASURE_WITH_UNIT(LENGTH_MEASURE(0.01),#45237,
'DISTANCE_ACCURACY_VALUE',
'Maximum model space distance between geometric entities at asserted c
onnectivities');
#45214=UNCERTAINTY_MEASURE_WITH_UNIT(LENGTH_MEASURE(0.01),#45237,
'DISTANCE_ACCURACY_VALUE',
'Maximum model space distance between geometric entities at asserted c
onnectivities');
#45222=(
GEOMETRIC_REPRESENTATION_CONTEXT(3)
GLOBAL_UNCERTAINTY_ASSIGNED_CONTEXT((#45200))
GLOBAL_UNIT_ASSIGNED_CONTEXT((#45237,#45239,#45240))
REPRESENTATION_CONTEXT('','3D')
);
#45236=(
GEOMETRIC_REPRESENTATION_CONTEXT(3)
GLOBAL_UNCERTAINTY_ASSIGNED_CONTEXT((#45214))
GLOBAL_UNIT_ASSIGNED_CONTEXT((#45237,#45239,#45240))
REPRESENTATION_CONTEXT('','3D')
);
#45237=(
LENGTH_UNIT()
NAMED_UNIT(*)
SI_UNIT(.MILLI.,.METRE.)
);
#45239=(
NAMED_UNIT(*)
PLANE_ANGLE_UNIT()
SI_UNIT($,.RADIAN.)
);
#45240=(
NAMED_UNIT(*)
SI_UNIT($,.STERADIAN.)
SOLID_ANGLE_UNIT()
);
#45248=SHAPE_DEFINITION_REPRESENTATION(#45269,#45320);
#45269=PRODUCT_DEFINITION_SHAPE('',$,#45342);
#45320=SHAPE_REPRESENTATION('',(#17165),#45222);
#45334=PRODUCT_DEFINITION_CONTEXT('part definition',#45399,'design');
#45342=PRODUCT_DEFINITION('2026-10-25-23-38-17-379',
'07_Die_Magnet_D6x5_NdFeB',#45363,#45334);
#45363=PRODUCT_DEFINITION_FORMATION('',$,#45408);
#45399=APPLICATION_CONTEXT(
'Core Data for Automotive Mechanical Design Process');
#45400=PRODUCT_CONTEXT('part definition',#45399,'mechanical');
#45408=PRODUCT('2026-10-25-23-38-17-379','07_Die_Magnet_D6x5_NdFeB',$,(#45400));
#45464=COLOUR_RGB('Light Blue',0.38,0.62,0.78);
#45465=FILL_AREA_STYLE_COLOUR('',#45464);
#45466=FILL_AREA_STYLE('',(#45465));
#45467=SURFACE_STYLE_FILL_AREA(#45466);
#45468=SURFACE_SIDE_STYLE('',(#45467));
#45469=SURFACE_STYLE_USAGE(.BOTH.,#45468);
#45470=PRESENTATION_STYLE_ASSIGNMENT((#45469));
ENDSEC;
END-ISO-10303-21;
